ISO-10303-21;
HEADER;
/* Generated by software containing ST-Developer
 * from STEP Tools, Inc. (www.steptools.com) 
 */

FILE_DESCRIPTION(
/* description */ ('Belt conveyor head drive unit'),
/* implementation_level */ '2;1');

FILE_NAME(
/* name */ 'M4 clamp nut (3).step',
/* time_stamp */ '2026-10-28T03:26:19-07:00',
/* author */ (''),
/* organization */ (''),
/* preprocessor_version */ 'ST-DEVELOPER v20.2',
/* originating_system */ 'Autodesk Translation Framework v15.17.0.0',
/* authorisation */ '');

FILE_SCHEMA (('AUTOMOTIVE_DESIGN { 1 0 10303 214 3 1 1 }'));
ENDSEC;

DATA;
#10=MECHANICAL_DESIGN_GEOMETRIC_PRESENTATION_REPRESENTATION('',(#858),#27069);
#720=SHAPE_REPRESENTATION_RELATIONSHIP('SRR','None',#27364,#789);
#789=ADVANCED_BREP_SHAPE_REPRESENTATION('',(#943),#27006);
#858=STYLED_ITEM('',(#27804),#943);
#943=MANIFOLD_SOLID_BREP('Body1',#13723);
#1082=FACE_BOUND('',#2654,.T.);
#1083=FACE_BOUND('',#2656,.T.);
#1354=PLANE('',#14876);
#1355=PLANE('',#14877);
#1781=FACE_OUTER_BOUND('',#2651,.T.);
#1782=FACE_OUTER_BOUND('',#2652,.T.);
#1783=FACE_OUTER_BOUND('',#2653,.T.);
#1784=FACE_OUTER_BOUND('',#2655,.T.);
#2651=EDGE_LOOP('',(#9630,#9631,#9632,#9633));
#2652=EDGE_LOOP('',(#9634,#9635,#9636,#9637));
#2653=EDGE_LOOP('',(#9638));
#2654=EDGE_LOOP('',(#9639));
#2655=EDGE_LOOP('',(#9640));
#2656=EDGE_LOOP('',(#9641));
#3688=LINE('',#21696,#4480);
#3689=LINE('',#21702,#4481);
#4480=VECTOR('',#17244,0.164999999999999);
#4481=VECTOR('',#17251,0.4);
#5228=CIRCLE('',#14871,0.164999999999999);
#5229=CIRCLE('',#14872,0.164999999999999);
#5230=CIRCLE('',#14874,0.4);
#5231=CIRCLE('',#14875,0.4);
#6177=VERTEX_POINT('',#21693);
#6178=VERTEX_POINT('',#21695);
#6179=VERTEX_POINT('',#21699);
#6180=VERTEX_POINT('',#21701);
#7507=EDGE_CURVE('',#6177,#6177,#5228,.T.);
#7508=EDGE_CURVE('',#6177,#6178,#3688,.T.);
#7509=EDGE_CURVE('',#6178,#6178,#5229,.T.);
#7510=EDGE_CURVE('',#6179,#6179,#5230,.T.);
#7511=EDGE_CURVE('',#6179,#6180,#3689,.T.);
#7512=EDGE_CURVE('',#6180,#6180,#5231,.T.);
#9630=ORIENTED_EDGE('',*,*,#7507,.F.);
#9631=ORIENTED_EDGE('',*,*,#7508,.T.);
#9632=ORIENTED_EDGE('',*,*,#7509,.T.);
#9633=ORIENTED_EDGE('',*,*,#7508,.F.);
#9634=ORIENTED_EDGE('',*,*,#7510,.F.);
#9635=ORIENTED_EDGE('',*,*,#7511,.T.);
#9636=ORIENTED_EDGE('',*,*,#7512,.T.);
#9637=ORIENTED_EDGE('',*,*,#7511,.F.);
#9638=ORIENTED_EDGE('',*,*,#7510,.T.);
#9639=ORIENTED_EDGE('',*,*,#7507,.T.);
#9640=ORIENTED_EDGE('',*,*,#7512,.F.);
#9641=ORIENTED_EDGE('',*,*,#7509,.F.);
#12603=CYLINDRICAL_SURFACE('',#14870,0.164999999999999);
#12604=CYLINDRICAL_SURFACE('',#14873,0.4);
#13060=ADVANCED_FACE('',(#1781),#12603,.F.);
#13061=ADVANCED_FACE('',(#1782),#12604,.T.);
#13062=ADVANCED_FACE('',(#1783,#1082),#1354,.T.);
#13063=ADVANCED_FACE('',(#1784,#1083),#1355,.F.);
#13723=CLOSED_SHELL('',(#13060,#13061,#13062,#13063));
#14869=AXIS2_PLACEMENT_3D('',#21691,#17238,#17239);
#14870=AXIS2_PLACEMENT_3D('',#21692,#17240,#17241);
#14871=AXIS2_PLACEMENT_3D('',#21694,#17242,#17243);
#14872=AXIS2_PLACEMENT_3D('',#21697,#17245,#17246);
#14873=AXIS2_PLACEMENT_3D('',#21698,#17247,#17248);
#14874=AXIS2_PLACEMENT_3D('',#21700,#17249,#17250);
#14875=AXIS2_PLACEMENT_3D('',#21703,#17252,#17253);
#14876=AXIS2_PLACEMENT_3D('',#21704,#17254,#17255);
#14877=AXIS2_PLACEMENT_3D('',#21705,#17256,#17257);
#17238=DIRECTION('axis',(0.,0.,1.));
#17239=DIRECTION('refdir',(1.,0.,0.));
#17240=DIRECTION('center_axis',(0.,0.,1.));
#17241=DIRECTION('ref_axis',(1.,0.,0.));
#17242=DIRECTION('center_axis',(0.,0.,-1.));
#17243=DIRECTION('ref_axis',(1.,0.,0.));
#17244=DIRECTION('',(0.,0.,-1.));
#17245=DIRECTION('center_axis',(0.,0.,-1.));
#17246=DIRECTION('ref_axis',(1.,0.,0.));
#17247=DIRECTION('center_axis',(0.,0.,1.));
#17248=DIRECTION('ref_axis',(1.,0.,0.));
#17249=DIRECTION('center_axis',(0.,0.,1.));
#17250=DIRECTION('ref_axis',(1.,0.,0.));
#17251=DIRECTION('',(0.,0.,-1.));
#17252=DIRECTION('center_axis',(0.,0.,1.));
#17253=DIRECTION('ref_axis',(1.,0.,0.));
#17254=DIRECTION('center_axis',(0.,0.,1.));
#17255=DIRECTION('ref_axis',(1.,0.,0.));
#17256=DIRECTION('center_axis',(0.,0.,1.));
#17257=DIRECTION('ref_axis',(1.,0.,0.));
#21691=CARTESIAN_POINT('',(0.,0.,0.));
#21692=CARTESIAN_POINT('Origin',(9.77091003018116,1.,-1.6));
#21693=CARTESIAN_POINT('',(9.60591003018116,1.,-1.2));
#21694=CARTESIAN_POINT('Origin',(9.77091003018116,1.,-1.2));
#21695=CARTESIAN_POINT('',(9.60591003018116,1.,-1.6));
#21696=CARTESIAN_POINT('',(9.60591003018116,1.,-1.6));
#21697=CARTESIAN_POINT('Origin',(9.77091003018116,1.,-1.6));
#21698=CARTESIAN_POINT('Origin',(9.77091003018116,1.,-1.6));
#21699=CARTESIAN_POINT('',(9.37091003018116,1.,-1.2));
#21700=CARTESIAN_POINT('Origin',(9.77091003018116,1.,-1.2));
#21701=CARTESIAN_POINT('',(9.37091003018116,1.,-1.6));
#21702=CARTESIAN_POINT('',(9.37091003018116,1.,-1.6));
#21703=CARTESIAN_POINT('Origin',(9.77091003018116,1.,-1.6));
#21704=CARTESIAN_POINT('Origin',(9.77091003018116,1.,-1.2));
#21705=CARTESIAN_POINT('Origin',(9.77091003018116,1.,-1.6));
#26929=UNCERTAINTY_MEASURE_WITH_UNIT(LENGTH_MEASURE(0.001),#27070,
'DISTANCE_ACCURACY_VALUE',
'Maximum model space distance between geometric entities at asserted c
onnectivities');
#26992=UNCERTAINTY_MEASURE_WITH_UNIT(LENGTH_MEASURE(0.001),#27070,
'DISTANCE_ACCURACY_VALUE',
'Maximum model space distance between geometric entities at asserted c
onnectivities');
#27006=(
GEOMETRIC_REPRESENTATION_CONTEXT(3)
GLOBAL_UNCERTAINTY_ASSIGNED_CONTEXT((#26929))
GLOBAL_UNIT_ASSIGNED_CONTEXT((#27070,#27072,#27073))
REPRESENTATION_CONTEXT('','3D')
);
#27069=(
GEOMETRIC_REPRESENTATION_CONTEXT(3)
GLOBAL_UNCERTAINTY_ASSIGNED_CONTEXT((#26992))
GLOBAL_UNIT_ASSIGNED_CONTEXT((#27070,#27072,#27073))
REPRESENTATION_CONTEXT('','3D')
);
#27070=(
LENGTH_UNIT()
NAMED_UNIT(*)
SI_UNIT(.CENTI.,.METRE.)
);
#27072=(
NAMED_UNIT(*)
PLANE_ANGLE_UNIT()
SI_UNIT($,.RADIAN.)
);
#27073=(
NAMED_UNIT(*)
SI_UNIT($,.STERADIAN.)
SOLID_ANGLE_UNIT()
);
#27087=SHAPE_DEFINITION_REPRESENTATION(#27163,#27364);
#27163=PRODUCT_DEFINITION_SHAPE('',$,#27441);
#27364=SHAPE_REPRESENTATION('',(#14869),#27006);
#27427=PRODUCT_DEFINITION_CONTEXT('part definition',#27657,'design');
#27441=PRODUCT_DEFINITION('M4 clamp nut (3)','M4 clamp nut (3)',#27517,#27427);
#27517=PRODUCT_DEFINITION_FORMATION('',$,#27672);
#27657=APPLICATION_CONTEXT(
'Core Data for Automotive Mechanical Design Process');
#27658=PRODUCT_CONTEXT('part definition',#27657,'mechanical');
#27672=PRODUCT('M4 clamp nut (3)','M4 clamp nut (3)','M4 clamp nut (3)',(#27658));
#27798=COLOUR_RGB('Black',0.12,0.14,0.17);
#27799=FILL_AREA_STYLE_COLOUR('',#27798);
#27800=FILL_AREA_STYLE('',(#27799));
#27801=SURFACE_STYLE_FILL_AREA(#27800);
#27802=SURFACE_SIDE_STYLE('',(#27801));
#27803=SURFACE_STYLE_USAGE(.BOTH.,#27802);
#27804=PRESENTATION_STYLE_ASSIGNMENT((#27803));
ENDSEC;
END-ISO-10303-21;
